ISO-10303-21;
HEADER;
FILE_DESCRIPTION (('STEP AP203'),
    '1' );
FILE_NAME ('Pin00.step',
    '2026-10-31T14:11:27',
    ( '' ),
    ( '' ),
    'SwSTEP 2.0',
    'SolidWorks 2024',
    '' );
FILE_SCHEMA (( 'AUTOMOTIVE_DESIGN' ));
ENDSEC;

DATA;
#353=SHAPE_REPRESENTATION_RELATIONSHIP ( 'NONE' , 'NONE' ,  #4456, #9686 ) ;
#415=DIRECTION ( 'NONE',  ( 1.000000000000000000, 0.000000000000000000, 0.000000000000000000 ) ) ;
#481=( NAMED_UNIT ( * ) SI_UNIT ( $, .STERADIAN. ) SOLID_ANGLE_UNIT ( ) );
#492=EDGE_LOOP ( 'NONE', ( #9352, #22717 ) ) ;
#788=ORIENTED_EDGE ( 'NONE', *, *, #11343, .T. ) ;
#959=CARTESIAN_POINT ( 'NONE',  ( 0.000000000000000000, 0.000000000000000000, -5.000000000000000000 ) ) ;
#1256=CYLINDRICAL_SURFACE ( 'NONE', #5343, 2.500000000000000000 ) ;
#1413=ADVANCED_FACE ( 'NONE', ( #20587 ), #20929, .T. ) ;
#1570=DIRECTION ( 'NONE',  ( 0.000000000000000000, -1.554450629062379680E-16, 1.000000000000000000 ) ) ;
#2569=CARTESIAN_POINT ( 'NONE',  ( 0.000000000000000000, 0.000000000000000000, 0.000000000000000000 ) ) ;
#2572=AXIS2_PLACEMENT_3D ( 'NONE', #959, #8217, #13673 ) ;
#3293=PRODUCT_DEFINITION ( 'UNKNOWN', '', #8400, #8526 ) ;
#3759=CARTESIAN_POINT ( 'NONE',  ( 3.061616997868382648E-16, -2.500000000000000000, -5.000000000000000000 ) ) ;
#3958=EDGE_LOOP ( 'NONE', ( #12760, #6293, #21946, #4189 ) ) ;
#4018=ORIENTED_EDGE ( 'NONE', *, *, #11258, .T. ) ;
#4189=ORIENTED_EDGE ( 'NONE', *, *, #16476, .F. ) ;
#4218=LINE ( 'NONE', #13485, #18709 ) ;
#4250=EDGE_CURVE ( 'NONE', #5973, #6701, #8465, .T. ) ;
#4456=SHAPE_REPRESENTATION ( 'Pin00', ( #12739 ), #10268 ) ;
#4713=DIRECTION ( 'NONE',  ( 0.000000000000000000, 0.000000000000000000, -1.000000000000000000 ) ) ;
#4732=CARTESIAN_POINT ( 'NONE',  ( 0.000000000000000000, 2.500000000000000000, -5.000000000000000000 ) ) ;
#4842=CIRCLE ( 'NONE', #2572, 2.500000000000000000 ) ;
#5041=DIRECTION ( 'NONE',  ( 0.000000000000000000, 0.000000000000000000, -1.000000000000000000 ) ) ;
#5343=AXIS2_PLACEMENT_3D ( 'NONE', #19314, #4713, #8395 ) ;
#5376=PLANE ( 'NONE',  #18877 ) ;
#5474=ORIENTED_EDGE ( 'NONE', *, *, #11343, .F. ) ;
#5973=VERTEX_POINT ( 'NONE', #12864 ) ;
#6125=CARTESIAN_POINT ( 'NONE',  ( 0.000000000000000000, 0.000000000000000000, -5.000000000000000000 ) ) ;
#6251=APPLICATION_CONTEXT ( 'configuration controlled 3d designs of mechanical parts and assemblies' ) ;
#6293=ORIENTED_EDGE ( 'NONE', *, *, #18777, .T. ) ;
#6429=DIRECTION ( 'NONE',  ( 0.000000000000000000, 1.000000000000000000, 0.000000000000000000 ) ) ;
#6559=CARTESIAN_POINT ( 'NONE',  ( 0.000000000000000000, -1.554450629062379975E-15, 5.000000000000000000 ) ) ;
#6701=VERTEX_POINT ( 'NONE', #15684 ) ;
#7038=LINE ( 'NONE', #21494, #14885 ) ;
#7166=ADVANCED_FACE ( 'NONE', ( #17529 ), #13851, .T. ) ;
#7509=CIRCLE ( 'NONE', #23406, 2.500000000000000000 ) ;
#7560=DIRECTION ( 'NONE',  ( 0.000000000000000000, 1.000000000000000000, 0.000000000000000000 ) ) ;
#8217=DIRECTION ( 'NONE',  ( 0.000000000000000000, 0.000000000000000000, -1.000000000000000000 ) ) ;
#8304=VERTEX_POINT ( 'NONE', #4732 ) ;
#8395=DIRECTION ( 'NONE',  ( 0.000000000000000000, 1.000000000000000000, 0.000000000000000000 ) ) ;
#8400=PRODUCT_DEFINITION_FORMATION_WITH_SPECIFIED_SOURCE ( 'ANY', '', #21217, .NOT_KNOWN. ) ;
#8465=CIRCLE ( 'NONE', #9986, 2.500000000000000000 ) ;
#8471=AXIS2_PLACEMENT_3D ( 'NONE', #21193, #13728, #20971 ) ;
#8526=DESIGN_CONTEXT ( 'detailed design', #19327, 'design' ) ;
#8951=FACE_OUTER_BOUND ( 'NONE', #492, .T. ) ;
#9094=MANIFOLD_SOLID_BREP ( 'Imported1', #15205 ) ;
#9352=ORIENTED_EDGE ( 'NONE', *, *, #4250, .F. ) ;
#9373=AXIS2_PLACEMENT_3D ( 'NONE', #6125, #18379, #7560 ) ;
#9686=ADVANCED_BREP_SHAPE_REPRESENTATION ( '', ( #9094, #12739 ), #10268 ) ;
#9932=DIRECTION ( 'NONE',  ( 0.000000000000000000, 0.000000000000000000, -1.000000000000000000 ) ) ;
#9986=AXIS2_PLACEMENT_3D ( 'NONE', #21300, #5041, #22714 ) ;
#10234=ADVANCED_FACE ( 'NONE', ( #14208 ), #1256, .T. ) ;
#10268=( GEOMETRIC_REPRESENTATION_CONTEXT ( 3 ) GLOBAL_UNCERTAINTY_ASSIGNED_CONTEXT ( ( #18206 ) ) GLOBAL_UNIT_ASSIGNED_CONTEXT ( ( #16749, #16514, #481 ) ) REPRESENTATION_CONTEXT ( 'NONE', 'WORKASPACE' ) );
#10916=ADVANCED_FACE ( 'NONE', ( #8951 ), #5376, .T. ) ;
#11258=EDGE_CURVE ( 'NONE', #6701, #5973, #7509, .T. ) ;
#11343=EDGE_CURVE ( 'NONE', #21585, #8304, #4842, .T. ) ;
#12739=AXIS2_PLACEMENT_3D ( 'NONE', #2569, #13380, #415 ) ;
#12760=ORIENTED_EDGE ( 'NONE', *, *, #4250, .T. ) ;
#12833=EDGE_LOOP ( 'NONE', ( #19322, #4018, #17200, #5474 ) ) ;
#12864=CARTESIAN_POINT ( 'NONE',  ( 0.000000000000000000, 2.499999999999998224, 5.000000000000000000 ) ) ;
#13380=DIRECTION ( 'NONE',  ( 0.000000000000000000, 0.000000000000000000, 1.000000000000000000 ) ) ;
#13485=CARTESIAN_POINT ( 'NONE',  ( 3.061616997868383141E-16, -2.500000000000000444, -2.500000000000000000 ) ) ;
#13673=DIRECTION ( 'NONE',  ( 0.000000000000000000, 1.000000000000000000, 0.000000000000000000 ) ) ;
#13691=DIRECTION ( 'NONE',  ( 0.000000000000000000, 0.000000000000000000, -1.000000000000000000 ) ) ;
#13728=DIRECTION ( 'NONE',  ( 0.000000000000000000, 1.554450629062379680E-16, -1.000000000000000000 ) ) ;
#13836=PRODUCT_DEFINITION_SHAPE ( 'NONE', 'NONE',  #3293 ) ;
#13851=PLANE ( 'NONE',  #8471 ) ;
#14208=FACE_OUTER_BOUND ( 'NONE', #12833, .T. ) ;
#14885=VECTOR ( 'NONE', #23385, 1000.000000000000000 ) ;
#15205=CLOSED_SHELL ( 'NONE', ( #1413, #10234, #7166, #10916 ) ) ;
#15684=CARTESIAN_POINT ( 'NONE',  ( 3.061616997868384620E-16, -2.500000000000001776, 5.000000000000000000 ) ) ;
#16476=EDGE_CURVE ( 'NONE', #5973, #8304, #7038, .T. ) ;
#16514=( NAMED_UNIT ( * ) PLANE_ANGLE_UNIT ( ) SI_UNIT ( $, .RADIAN. ) );
#16749=( LENGTH_UNIT ( ) NAMED_UNIT ( * ) SI_UNIT ( .MILLI., .METRE. ) );
#16945=CIRCLE ( 'NONE', #9373, 2.500000000000000000 ) ;
#17200=ORIENTED_EDGE ( 'NONE', *, *, #16476, .T. ) ;
#17482=ORIENTED_EDGE ( 'NONE', *, *, #22013, .T. ) ;
#17529=FACE_OUTER_BOUND ( 'NONE', #21823, .T. ) ;
#17586=MECHANICAL_CONTEXT ( 'NONE', #6251, 'mechanical' ) ;
#18089=CARTESIAN_POINT ( 'NONE',  ( 0.000000000000000000, 1.250000000000000000, 5.000000000000000000 ) ) ;
#18206=UNCERTAINTY_MEASURE_WITH_UNIT (LENGTH_MEASURE( 1.000000000000000082E-05 ), #16749, 'distance_accuracy_value', 'NONE');
#18379=DIRECTION ( 'NONE',  ( 0.000000000000000000, 0.000000000000000000, -1.000000000000000000 ) ) ;
#18709=VECTOR ( 'NONE', #9932, 1000.000000000000000 ) ;
#18777=EDGE_CURVE ( 'NONE', #6701, #21585, #4218, .T. ) ;
#18877=AXIS2_PLACEMENT_3D ( 'NONE', #18089, #1570, #20092 ) ;
#18927=CARTESIAN_POINT ( 'NONE',  ( 0.000000000000000000, -3.886126572655959799E-16, -2.500000000000000000 ) ) ;
#19314=CARTESIAN_POINT ( 'NONE',  ( 0.000000000000000000, -3.886126572655959799E-16, -2.500000000000000000 ) ) ;
#19322=ORIENTED_EDGE ( 'NONE', *, *, #18777, .F. ) ;
#19327=APPLICATION_CONTEXT ( 'configuration controlled 3d designs of mechanical parts and assemblies' ) ;
#20092=DIRECTION ( 'NONE',  ( 1.000000000000000000, 0.000000000000000000, 0.000000000000000000 ) ) ;
#20587=FACE_OUTER_BOUND ( 'NONE', #3958, .T. ) ;
#20929=CYLINDRICAL_SURFACE ( 'NONE', #21136, 2.500000000000000000 ) ;
#20971=DIRECTION ( 'NONE',  ( -1.000000000000000000, 0.000000000000000000, 0.000000000000000000 ) ) ;
#21055=DIRECTION ( 'NONE',  ( 0.000000000000000000, 1.000000000000000000, 0.000000000000000000 ) ) ;
#21136=AXIS2_PLACEMENT_3D ( 'NONE', #18927, #13691, #21055 ) ;
#21193=CARTESIAN_POINT ( 'NONE',  ( 0.000000000000000000, 1.250000000000000000, -5.000000000000000000 ) ) ;
#21217=PRODUCT ( 'Pin00', 'Pin00', '', ( #17586 ) ) ;
#21260=DIRECTION ( 'NONE',  ( 0.000000000000000000, 0.000000000000000000, -1.000000000000000000 ) ) ;
#21300=CARTESIAN_POINT ( 'NONE',  ( 0.000000000000000000, -1.554450629062379975E-15, 5.000000000000000000 ) ) ;
#21494=CARTESIAN_POINT ( 'NONE',  ( 0.000000000000000000, 2.499999999999999556, -2.500000000000000000 ) ) ;
#21585=VERTEX_POINT ( 'NONE', #3759 ) ;
#21820=SHAPE_DEFINITION_REPRESENTATION ( #13836, #4456 ) ;
#21823=EDGE_LOOP ( 'NONE', ( #17482, #788 ) ) ;
#21946=ORIENTED_EDGE ( 'NONE', *, *, #22013, .F. ) ;
#22013=EDGE_CURVE ( 'NONE', #8304, #21585, #16945, .T. ) ;
#22714=DIRECTION ( 'NONE',  ( 0.000000000000000000, 1.000000000000000000, 0.000000000000000000 ) ) ;
#22717=ORIENTED_EDGE ( 'NONE', *, *, #11258, .F. ) ;
#23385=DIRECTION ( 'NONE',  ( 0.000000000000000000, 0.000000000000000000, -1.000000000000000000 ) ) ;
#23406=AXIS2_PLACEMENT_3D ( 'NONE', #6559, #21260, #6429 ) ;
#23543=COLOUR_RGB('Light Gray', 0.72549020, 0.75294118, 0.79215686);
#23544=FILL_AREA_STYLE_COLOUR('',#23543);
#23545=FILL_AREA_STYLE('',(#23544));
#23546=SURFACE_STYLE_FILL_AREA(#23545);
#23547=SURFACE_SIDE_STYLE('',(#23546));
#23548=SURFACE_STYLE_USAGE(.BOTH.,#23547);
#23549=PRESENTATION_STYLE_ASSIGNMENT((#23548));
#23581=STYLED_ITEM('',(#23549),#9094);
#23582=MECHANICAL_DESIGN_GEOMETRIC_PRESENTATION_REPRESENTATION('',(#23581),#10268);
ENDSEC;
END-ISO-10303-21;
